ISO-10303-21;
HEADER;
/* Generated by software containing ST-Developer
 * from STEP Tools, Inc. (www.steptools.com) 
 */

FILE_DESCRIPTION(
/* description */ ('XY cross-slide table'),
/* implementation_level */ '2;1');

FILE_NAME(
/* name */ 'Cap Screw - M5x20 (1).step',
/* time_stamp */ '2026-10-28T03:22:46-07:00',
/* author */ (''),
/* organization */ (''),
/* preprocessor_version */ 'ST-DEVELOPER v20.2',
/* originating_system */ 'Autodesk Translation Framework v15.17.0.0',
/* authorisation */ '');

FILE_SCHEMA (('AUTOMOTIVE_DESIGN { 1 0 10303 214 3 1 1 }'));
ENDSEC;

DATA;
#10=MECHANICAL_DESIGN_GEOMETRIC_PRESENTATION_REPRESENTATION('',(#1772),#62984);
#26=ORIENTED_CLOSED_SHELL('',*,#23074,.F.);
#35=BREP_WITH_VOIDS('Body1',#23073,(#26));
#1486=CONICAL_SURFACE('',#26083,0.4,0.785398163397448);
#1487=CONICAL_SURFACE('',#26087,0.41,0.785398163397448);
#1488=CONICAL_SURFACE('',#26091,0.26,0.463647609000806);
#1489=CONICAL_SURFACE('',#26095,0.225,0.785398163397448);
#1576=SHAPE_REPRESENTATION_RELATIONSHIP('SRR','None',#63435,#1659);
#1659=ADVANCED_BREP_SHAPE_REPRESENTATION('',(#35),#62972);
#1772=STYLED_ITEM('',(#63919),#35);
#2271=FACE_BOUND('',#5651,.T.);
#2798=PLANE('',#26081);
#2799=PLANE('',#26089);
#2800=PLANE('',#26097);
#2801=PLANE('',#26098);
#2802=PLANE('',#26099);
#2803=PLANE('',#26100);
#2804=PLANE('',#26101);
#2805=PLANE('',#26102);
#2806=PLANE('',#26103);
#2807=PLANE('',#26104);
#2808=PLANE('',#26105);
#3948=FACE_OUTER_BOUND('',#5646,.T.);
#3949=FACE_OUTER_BOUND('',#5647,.T.);
#3950=FACE_OUTER_BOUND('',#5648,.T.);
#3951=FACE_OUTER_BOUND('',#5649,.T.);
#3952=FACE_OUTER_BOUND('',#5650,.T.);
#3953=FACE_OUTER_BOUND('',#5652,.T.);
#3954=FACE_OUTER_BOUND('',#5653,.T.);
#3955=FACE_OUTER_BOUND('',#5654,.T.);
#3956=FACE_OUTER_BOUND('',#5655,.T.);
#3957=FACE_OUTER_BOUND('',#5656,.T.);
#3958=FACE_OUTER_BOUND('',#5657,.T.);
#3959=FACE_OUTER_BOUND('',#5658,.T.);
#3960=FACE_OUTER_BOUND('',#5659,.T.);
#3961=FACE_OUTER_BOUND('',#5660,.T.);
#3962=FACE_OUTER_BOUND('',#5661,.T.);
#3963=FACE_OUTER_BOUND('',#5662,.T.);
#3964=FACE_OUTER_BOUND('',#5663,.T.);
#5646=EDGE_LOOP('',(#19844));
#5647=EDGE_LOOP('',(#19845,#19846,#19847,#19848));
#5648=EDGE_LOOP('',(#19849,#19850,#19851,#19852));
#5649=EDGE_LOOP('',(#19853,#19854,#19855,#19856));
#5650=EDGE_LOOP('',(#19857));
#5651=EDGE_LOOP('',(#19858));
#5652=EDGE_LOOP('',(#19859,#19860,#19861,#19862));
#5653=EDGE_LOOP('',(#19863,#19864,#19865,#19866));
#5654=EDGE_LOOP('',(#19867,#19868,#19869,#19870));
#5655=EDGE_LOOP('',(#19871));
#5656=EDGE_LOOP('',(#19872,#19873,#19874,#19875));
#5657=EDGE_LOOP('',(#19876,#19877,#19878,#19879));
#5658=EDGE_LOOP('',(#19880,#19881,#19882,#19883));
#5659=EDGE_LOOP('',(#19884,#19885,#19886,#19887));
#5660=EDGE_LOOP('',(#19888,#19889,#19890,#19891));
#5661=EDGE_LOOP('',(#19892,#19893,#19894,#19895));
#5662=EDGE_LOOP('',(#19896,#19897,#19898,#19899,#19900,#19901));
#5663=EDGE_LOOP('',(#19902,#19903,#19904,#19905,#19906,#19907));
#7129=LINE('',#52538,#8616);
#7130=LINE('',#52542,#8617);
#7131=LINE('',#52546,#8618);
#7132=LINE('',#52553,#8619);
#7133=LINE('',#52557,#8620);
#7134=LINE('',#52561,#8621);
#7135=LINE('',#52566,#8622);
#7136=LINE('',#52568,#8623);
#7137=LINE('',#52570,#8624);
#7138=LINE('',#52571,#8625);
#7139=LINE('',#52574,#8626);
#7140=LINE('',#52576,#8627);
#7141=LINE('',#52577,#8628);
#7142=LINE('',#52580,#8629);
#7143=LINE('',#52582,#8630);
#7144=LINE('',#52583,#8631);
#7145=LINE('',#52586,#8632);
#7146=LINE('',#52588,#8633);
#7147=LINE('',#52589,#8634);
#7148=LINE('',#52592,#8635);
#7149=LINE('',#52594,#8636);
#7150=LINE('',#52595,#8637);
#7151=LINE('',#52597,#8638);
#7152=LINE('',#52598,#8639);
#8616=VECTOR('',#31854,0.4);
#8617=VECTOR('',#31859,0.425);
#8618=VECTOR('',#31864,0.41);
#8619=VECTOR('',#31873,0.26);
#8620=VECTOR('',#31878,0.25);
#8621=VECTOR('',#31883,0.225);
#8622=VECTOR('',#31888,1.);
#8623=VECTOR('',#31889,1.);
#8624=VECTOR('',#31890,1.);
#8625=VECTOR('',#31891,1.);
#8626=VECTOR('',#31894,1.);
#8627=VECTOR('',#31895,1.);
#8628=VECTOR('',#31896,1.);
#8629=VECTOR('',#31899,1.);
#8630=VECTOR('',#31900,1.);
#8631=VECTOR('',#31901,1.);
#8632=VECTOR('',#31904,1.);
#8633=VECTOR('',#31905,1.);
#8634=VECTOR('',#31906,1.);
#8635=VECTOR('',#31909,1.);
#8636=VECTOR('',#31910,1.);
#8637=VECTOR('',#31911,1.);
#8638=VECTOR('',#31914,1.);
#8639=VECTOR('',#31915,1.);
#9708=CIRCLE('',#26082,0.375);
#9709=CIRCLE('',#26084,0.425);
#9710=CIRCLE('',#26086,0.425);
#9711=CIRCLE('',#26088,0.395);
#9712=CIRCLE('',#26090,0.27);
#9713=CIRCLE('',#26092,0.24505);
#9714=CIRCLE('',#26094,0.24505);
#9715=CIRCLE('',#26096,0.2);
#11440=VERTEX_POINT('',#52533);
#11441=VERTEX_POINT('',#52536);
#11442=VERTEX_POINT('',#52540);
#11443=VERTEX_POINT('',#52544);
#11444=VERTEX_POINT('',#52548);
#11445=VERTEX_POINT('',#52551);
#11446=VERTEX_POINT('',#52555);
#11447=VERTEX_POINT('',#52559);
#11448=VERTEX_POINT('',#52564);
#11449=VERTEX_POINT('',#52565);
#11450=VERTEX_POINT('',#52567);
#11451=VERTEX_POINT('',#52569);
#11452=VERTEX_POINT('',#52573);
#11453=VERTEX_POINT('',#52575);
#11454=VERTEX_POINT('',#52579);
#11455=VERTEX_POINT('',#52581);
#11456=VERTEX_POINT('',#52585);
#11457=VERTEX_POINT('',#52587);
#11458=VERTEX_POINT('',#52591);
#11459=VERTEX_POINT('',#52593);
#14306=EDGE_CURVE('',#11440,#11440,#9708,.T.);
#14307=EDGE_CURVE('',#11441,#11441,#9709,.T.);
#14308=EDGE_CURVE('',#11441,#11440,#7129,.T.);
#14309=EDGE_CURVE('',#11442,#11442,#9710,.T.);
#14310=EDGE_CURVE('',#11442,#11441,#7130,.T.);
#14311=EDGE_CURVE('',#11443,#11443,#9711,.T.);
#14312=EDGE_CURVE('',#11443,#11442,#7131,.T.);
#14313=EDGE_CURVE('',#11444,#11444,#9712,.T.);
#14314=EDGE_CURVE('',#11445,#11445,#9713,.F.);
#14315=EDGE_CURVE('',#11445,#11444,#7132,.T.);
#14316=EDGE_CURVE('',#11446,#11446,#9714,.F.);
#14317=EDGE_CURVE('',#11446,#11445,#7133,.T.);
#14318=EDGE_CURVE('',#11447,#11447,#9715,.T.);
#14319=EDGE_CURVE('',#11447,#11446,#7134,.T.);
#14320=EDGE_CURVE('',#11448,#11449,#7135,.T.);
#14321=EDGE_CURVE('',#11449,#11450,#7136,.T.);
#14322=EDGE_CURVE('',#11450,#11451,#7137,.T.);
#14323=EDGE_CURVE('',#11448,#11451,#7138,.T.);
#14324=EDGE_CURVE('',#11449,#11452,#7139,.T.);
#14325=EDGE_CURVE('',#11452,#11453,#7140,.T.);
#14326=EDGE_CURVE('',#11453,#11450,#7141,.T.);
#14327=EDGE_CURVE('',#11452,#11454,#7142,.T.);
#14328=EDGE_CURVE('',#11454,#11455,#7143,.T.);
#14329=EDGE_CURVE('',#11455,#11453,#7144,.T.);
#14330=EDGE_CURVE('',#11454,#11456,#7145,.T.);
#14331=EDGE_CURVE('',#11456,#11457,#7146,.T.);
#14332=EDGE_CURVE('',#11457,#11455,#7147,.T.);
#14333=EDGE_CURVE('',#11456,#11458,#7148,.T.);
#14334=EDGE_CURVE('',#11458,#11459,#7149,.T.);
#14335=EDGE_CURVE('',#11459,#11457,#7150,.T.);
#14336=EDGE_CURVE('',#11458,#11448,#7151,.T.);
#14337=EDGE_CURVE('',#11451,#11459,#7152,.T.);
#19844=ORIENTED_EDGE('',*,*,#14306,.F.);
#19845=ORIENTED_EDGE('',*,*,#14307,.F.);
#19846=ORIENTED_EDGE('',*,*,#14308,.T.);
#19847=ORIENTED_EDGE('',*,*,#14306,.T.);
#19848=ORIENTED_EDGE('',*,*,#14308,.F.);
#19849=ORIENTED_EDGE('',*,*,#14309,.F.);
#19850=ORIENTED_EDGE('',*,*,#14310,.T.);
#19851=ORIENTED_EDGE('',*,*,#14307,.T.);
#19852=ORIENTED_EDGE('',*,*,#14310,.F.);
#19853=ORIENTED_EDGE('',*,*,#14311,.F.);
#19854=ORIENTED_EDGE('',*,*,#14312,.T.);
#19855=ORIENTED_EDGE('',*,*,#14309,.T.);
#19856=ORIENTED_EDGE('',*,*,#14312,.F.);
#19857=ORIENTED_EDGE('',*,*,#14311,.T.);
#19858=ORIENTED_EDGE('',*,*,#14313,.F.);
#19859=ORIENTED_EDGE('',*,*,#14314,.F.);
#19860=ORIENTED_EDGE('',*,*,#14315,.T.);
#19861=ORIENTED_EDGE('',*,*,#14313,.T.);
#19862=ORIENTED_EDGE('',*,*,#14315,.F.);
#19863=ORIENTED_EDGE('',*,*,#14316,.F.);
#19864=ORIENTED_EDGE('',*,*,#14317,.T.);
#19865=ORIENTED_EDGE('',*,*,#14314,.T.);
#19866=ORIENTED_EDGE('',*,*,#14317,.F.);
#19867=ORIENTED_EDGE('',*,*,#14318,.F.);
#19868=ORIENTED_EDGE('',*,*,#14319,.T.);
#19869=ORIENTED_EDGE('',*,*,#14316,.T.);
#19870=ORIENTED_EDGE('',*,*,#14319,.F.);
#19871=ORIENTED_EDGE('',*,*,#14318,.T.);
#19872=ORIENTED_EDGE('',*,*,#14320,.T.);
#19873=ORIENTED_EDGE('',*,*,#14321,.T.);
#19874=ORIENTED_EDGE('',*,*,#14322,.T.);
#19875=ORIENTED_EDGE('',*,*,#14323,.F.);
#19876=ORIENTED_EDGE('',*,*,#14324,.T.);
#19877=ORIENTED_EDGE('',*,*,#14325,.T.);
#19878=ORIENTED_EDGE('',*,*,#14326,.T.);
#19879=ORIENTED_EDGE('',*,*,#14321,.F.);
#19880=ORIENTED_EDGE('',*,*,#14327,.T.);
#19881=ORIENTED_EDGE('',*,*,#14328,.T.);
#19882=ORIENTED_EDGE('',*,*,#14329,.T.);
#19883=ORIENTED_EDGE('',*,*,#14325,.F.);
#19884=ORIENTED_EDGE('',*,*,#14330,.T.);
#19885=ORIENTED_EDGE('',*,*,#14331,.T.);
#19886=ORIENTED_EDGE('',*,*,#14332,.T.);
#19887=ORIENTED_EDGE('',*,*,#14328,.F.);
#19888=ORIENTED_EDGE('',*,*,#14333,.T.);
#19889=ORIENTED_EDGE('',*,*,#14334,.T.);
#19890=ORIENTED_EDGE('',*,*,#14335,.T.);
#19891=ORIENTED_EDGE('',*,*,#14331,.F.);
#19892=ORIENTED_EDGE('',*,*,#14336,.T.);
#19893=ORIENTED_EDGE('',*,*,#14323,.T.);
#19894=ORIENTED_EDGE('',*,*,#14337,.T.);
#19895=ORIENTED_EDGE('',*,*,#14334,.F.);
#19896=ORIENTED_EDGE('',*,*,#14336,.F.);
#19897=ORIENTED_EDGE('',*,*,#14333,.F.);
#19898=ORIENTED_EDGE('',*,*,#14330,.F.);
#19899=ORIENTED_EDGE('',*,*,#14327,.F.);
#19900=ORIENTED_EDGE('',*,*,#14324,.F.);
#19901=ORIENTED_EDGE('',*,*,#14320,.F.);
#19902=ORIENTED_EDGE('',*,*,#14337,.F.);
#19903=ORIENTED_EDGE('',*,*,#14322,.F.);
#19904=ORIENTED_EDGE('',*,*,#14326,.F.);
#19905=ORIENTED_EDGE('',*,*,#14329,.F.);
#19906=ORIENTED_EDGE('',*,*,#14332,.F.);
#19907=ORIENTED_EDGE('',*,*,#14335,.F.);
#21498=CYLINDRICAL_SURFACE('',#26085,0.425);
#21499=CYLINDRICAL_SURFACE('',#26093,0.24505);
#22729=ADVANCED_FACE('',(#3948),#2798,.T.);
#22730=ADVANCED_FACE('',(#3949),#1486,.T.);
#22731=ADVANCED_FACE('',(#3950),#21498,.T.);
#22732=ADVANCED_FACE('',(#3951),#1487,.T.);
#22733=ADVANCED_FACE('',(#3952,#2271),#2799,.T.);
#22734=ADVANCED_FACE('',(#3953),#1488,.T.);
#22735=ADVANCED_FACE('',(#3954),#21499,.T.);
#22736=ADVANCED_FACE('',(#3955),#1489,.T.);
#22737=ADVANCED_FACE('',(#3956),#2800,.T.);
#22738=ADVANCED_FACE('',(#3957),#2801,.F.);
#22739=ADVANCED_FACE('',(#3958),#2802,.F.);
#22740=ADVANCED_FACE('',(#3959),#2803,.F.);
#22741=ADVANCED_FACE('',(#3960),#2804,.F.);
#22742=ADVANCED_FACE('',(#3961),#2805,.F.);
#22743=ADVANCED_FACE('',(#3962),#2806,.F.);
#22744=ADVANCED_FACE('',(#3963),#2807,.F.);
#22745=ADVANCED_FACE('',(#3964),#2808,.F.);
#23073=CLOSED_SHELL('',(#22729,#22730,#22731,#22732,#22733,#22734,#22735,
#22736,#22737));
#23074=CLOSED_SHELL('',(#22738,#22739,#22740,#22741,#22742,#22743,#22744,
#22745));
#26080=AXIS2_PLACEMENT_3D('',#52531,#31844,#31845);
#26081=AXIS2_PLACEMENT_3D('',#52532,#31846,#31847);
#26082=AXIS2_PLACEMENT_3D('',#52534,#31848,#31849);
#26083=AXIS2_PLACEMENT_3D('',#52535,#31850,#31851);
#26084=AXIS2_PLACEMENT_3D('',#52537,#31852,#31853);
#26085=AXIS2_PLACEMENT_3D('',#52539,#31855,#31856);
#26086=AXIS2_PLACEMENT_3D('',#52541,#31857,#31858);
#26087=AXIS2_PLACEMENT_3D('',#52543,#31860,#31861);
#26088=AXIS2_PLACEMENT_3D('',#52545,#31862,#31863);
#26089=AXIS2_PLACEMENT_3D('',#52547,#31865,#31866);
#26090=AXIS2_PLACEMENT_3D('',#52549,#31867,#31868);
#26091=AXIS2_PLACEMENT_3D('',#52550,#31869,#31870);
#26092=AXIS2_PLACEMENT_3D('',#52552,#31871,#31872);
#26093=AXIS2_PLACEMENT_3D('',#52554,#31874,#31875);
#26094=AXIS2_PLACEMENT_3D('',#52556,#31876,#31877);
#26095=AXIS2_PLACEMENT_3D('',#52558,#31879,#31880);
#26096=AXIS2_PLACEMENT_3D('',#52560,#31881,#31882);
#26097=AXIS2_PLACEMENT_3D('',#52562,#31884,#31885);
#26098=AXIS2_PLACEMENT_3D('',#52563,#31886,#31887);
#26099=AXIS2_PLACEMENT_3D('',#52572,#31892,#31893);
#26100=AXIS2_PLACEMENT_3D('',#52578,#31897,#31898);
#26101=AXIS2_PLACEMENT_3D('',#52584,#31902,#31903);
#26102=AXIS2_PLACEMENT_3D('',#52590,#31907,#31908);
#26103=AXIS2_PLACEMENT_3D('',#52596,#31912,#31913);
#26104=AXIS2_PLACEMENT_3D('',#52599,#31916,#31917);
#26105=AXIS2_PLACEMENT_3D('',#52600,#31918,#31919);
#31844=DIRECTION('axis',(0.,0.,1.));
#31845=DIRECTION('refdir',(1.,0.,0.));
#31846=DIRECTION('center_axis',(0.,1.,0.));
#31847=DIRECTION('ref_axis',(0.,0.,1.));
#31848=DIRECTION('center_axis',(0.,-1.,0.));
#31849=DIRECTION('ref_axis',(1.,0.,0.));
#31850=DIRECTION('center_axis',(0.,-1.,0.));
#31851=DIRECTION('ref_axis',(1.,0.,0.));
#31852=DIRECTION('center_axis',(0.,-1.,0.));
#31853=DIRECTION('ref_axis',(1.,0.,0.));
#31854=DIRECTION('',(0.707106781186548,0.707106781186547,8.65956056235493E-17));
#31855=DIRECTION('center_axis',(0.,-1.,0.));
#31856=DIRECTION('ref_axis',(1.,0.,0.));
#31857=DIRECTION('center_axis',(0.,-1.,0.));
#31858=DIRECTION('ref_axis',(1.,0.,0.));
#31859=DIRECTION('',(0.,1.,0.));
#31860=DIRECTION('center_axis',(0.,1.,0.));
#31861=DIRECTION('ref_axis',(1.,0.,0.));
#31862=DIRECTION('center_axis',(0.,-1.,0.));
#31863=DIRECTION('ref_axis',(1.,0.,0.));
#31864=DIRECTION('',(-0.707106781186547,0.707106781186548,-8.65956056235493E-17));
#31865=DIRECTION('center_axis',(0.,-1.,0.));
#31866=DIRECTION('ref_axis',(0.,0.,-1.));
#31867=DIRECTION('center_axis',(0.,-1.,0.));
#31868=DIRECTION('ref_axis',(1.,0.,0.));
#31869=DIRECTION('center_axis',(0.,1.,0.));
#31870=DIRECTION('ref_axis',(1.,0.,0.));
#31871=DIRECTION('center_axis',(0.,1.,0.));
#31872=DIRECTION('ref_axis',(1.,0.,0.));
#31873=DIRECTION('',(-0.447213595499958,0.894427190999916,-5.47678698264203E-17));
#31874=DIRECTION('center_axis',(0.,-1.,0.));
#31875=DIRECTION('ref_axis',(1.,0.,0.));
#31876=DIRECTION('center_axis',(0.,1.,0.));
#31877=DIRECTION('ref_axis',(1.,0.,0.));
#31878=DIRECTION('',(0.,1.,0.));
#31879=DIRECTION('center_axis',(0.,1.,0.));
#31880=DIRECTION('ref_axis',(1.,0.,0.));
#31881=DIRECTION('center_axis',(0.,-1.,0.));
#31882=DIRECTION('ref_axis',(1.,0.,0.));
#31883=DIRECTION('',(-0.707106781186547,0.707106781186548,-8.65956056235493E-17));
#31884=DIRECTION('center_axis',(0.,-1.,0.));
#31885=DIRECTION('ref_axis',(0.,0.,-1.));
#31886=DIRECTION('center_axis',(0.866025403784439,0.,-0.5));
#31887=DIRECTION('ref_axis',(0.5,0.,0.866025403784439));
#31888=DIRECTION('',(-0.5,0.,-0.866025403784439));
#31889=DIRECTION('',(0.,-1.,0.));
#31890=DIRECTION('',(0.5,0.,0.866025403784439));
#31891=DIRECTION('',(0.,-1.,0.));
#31892=DIRECTION('center_axis',(1.20185167898973E-16,0.,-1.));
#31893=DIRECTION('ref_axis',(1.,0.,1.20185167898973E-16));
#31894=DIRECTION('',(-1.,0.,-1.20185167898973E-16));
#31895=DIRECTION('',(0.,-1.,0.));
#31896=DIRECTION('',(1.,0.,1.20185167898973E-16));
#31897=DIRECTION('center_axis',(-0.866025403784439,0.,-0.5));
#31898=DIRECTION('ref_axis',(0.5,0.,-0.866025403784439));
#31899=DIRECTION('',(-0.5,0.,0.866025403784439));
#31900=DIRECTION('',(0.,-1.,0.));
#31901=DIRECTION('',(0.5,0.,-0.866025403784439));
#31902=DIRECTION('center_axis',(-0.866025403784439,0.,0.5));
#31903=DIRECTION('ref_axis',(-0.5,0.,-0.866025403784439));
#31904=DIRECTION('',(0.5,0.,0.866025403784439));
#31905=DIRECTION('',(0.,-1.,0.));
#31906=DIRECTION('',(-0.5,0.,-0.866025403784439));
#31907=DIRECTION('center_axis',(-2.40370335797945E-16,0.,1.));
#31908=DIRECTION('ref_axis',(-1.,0.,-2.40370335797945E-16));
#31909=DIRECTION('',(1.,0.,2.40370335797945E-16));
#31910=DIRECTION('',(0.,-1.,0.));
#31911=DIRECTION('',(-1.,0.,-2.40370335797945E-16));
#31912=DIRECTION('center_axis',(0.866025403784439,0.,0.5));
#31913=DIRECTION('ref_axis',(-0.5,0.,0.866025403784439));
#31914=DIRECTION('',(0.5,0.,-0.866025403784439));
#31915=DIRECTION('',(-0.5,0.,0.866025403784439));
#31916=DIRECTION('center_axis',(0.,1.,0.));
#31917=DIRECTION('ref_axis',(1.,0.,0.));
#31918=DIRECTION('center_axis',(0.,-1.,0.));
#31919=DIRECTION('ref_axis',(0.,0.,-1.));
#52531=CARTESIAN_POINT('',(0.,0.,0.));
#52532=CARTESIAN_POINT('Origin',(0.375,0.5,0.));
#52533=CARTESIAN_POINT('',(-0.375,0.5,-4.59242549680257E-17));
#52534=CARTESIAN_POINT('Origin',(0.,0.5,0.));
#52535=CARTESIAN_POINT('Origin',(0.,0.475,0.));
#52536=CARTESIAN_POINT('',(-0.425,0.45,-5.20474889637625E-17));
#52537=CARTESIAN_POINT('Origin',(0.,0.45,0.));
#52538=CARTESIAN_POINT('',(-0.4,0.475,-4.89858719658941E-17));
#52539=CARTESIAN_POINT('Origin',(0.,0.24,0.));
#52540=CARTESIAN_POINT('',(-0.425,0.0299999999999998,-5.20474889637625E-17));
#52541=CARTESIAN_POINT('Origin',(0.,0.0299999999999998,0.));
#52542=CARTESIAN_POINT('',(-0.425,0.24,-5.20474889637625E-17));
#52543=CARTESIAN_POINT('Origin',(0.,0.0150000000000001,0.));
#52544=CARTESIAN_POINT('',(-0.395,4.85722573273506E-17,-4.83735485663204E-17));
#52545=CARTESIAN_POINT('Origin',(0.,0.,0.));
#52546=CARTESIAN_POINT('',(-0.41,0.0150000000000001,-5.02105187650415E-17));
#52547=CARTESIAN_POINT('Origin',(0.27,0.,0.));
#52548=CARTESIAN_POINT('',(-0.27,0.,-3.30654635769785E-17));
#52549=CARTESIAN_POINT('Origin',(0.,0.,0.));
#52550=CARTESIAN_POINT('Origin',(0.,-0.02,0.));
#52551=CARTESIAN_POINT('',(-0.24505,-0.0498999999999999,3.00099698131059E-17));
#52552=CARTESIAN_POINT('Origin',(0.,-0.0498999999999999,0.));
#52553=CARTESIAN_POINT('',(-0.26,-0.02,-3.18408167778312E-17));
#52554=CARTESIAN_POINT('Origin',(0.,-0.995,0.));
#52555=CARTESIAN_POINT('',(-0.24505,-1.95495,3.00099698131059E-17));
#52556=CARTESIAN_POINT('Origin',(0.,-1.95495,0.));
#52557=CARTESIAN_POINT('',(-0.24505,-0.995,-3.00099698131059E-17));
#52558=CARTESIAN_POINT('Origin',(0.,-1.975,0.));
#52559=CARTESIAN_POINT('',(-0.2,-2.,-2.44929359829471E-17));
#52560=CARTESIAN_POINT('Origin',(0.,-2.,0.));
#52561=CARTESIAN_POINT('',(-0.225,-1.975,-2.75545529808154E-17));
#52562=CARTESIAN_POINT('Origin',(0.,-2.,0.));
#52563=CARTESIAN_POINT('Origin',(0.115470053837925,-0.5,-0.2));
#52564=CARTESIAN_POINT('',(0.23094010767585,-0.5,0.));
#52565=CARTESIAN_POINT('',(0.115470053837925,-0.5,-0.2));
#52566=CARTESIAN_POINT('',(0.23094010767585,-0.5,0.));
#52567=CARTESIAN_POINT('',(0.115470053837925,-0.8,-0.2));
#52568=CARTESIAN_POINT('',(0.115470053837925,-0.5,-0.2));
#52569=CARTESIAN_POINT('',(0.23094010767585,-0.8,0.));
#52570=CARTESIAN_POINT('',(0.23094010767585,-0.8,0.));
#52571=CARTESIAN_POINT('',(0.23094010767585,-0.5,0.));
#52572=CARTESIAN_POINT('Origin',(-0.115470053837925,-0.5,-0.2));
#52573=CARTESIAN_POINT('',(-0.115470053837925,-0.5,-0.2));
#52574=CARTESIAN_POINT('',(0.115470053837925,-0.5,-0.2));
#52575=CARTESIAN_POINT('',(-0.115470053837925,-0.8,-0.2));
#52576=CARTESIAN_POINT('',(-0.115470053837925,-0.5,-0.2));
#52577=CARTESIAN_POINT('',(0.115470053837925,-0.8,-0.2));
#52578=CARTESIAN_POINT('Origin',(-0.23094010767585,-0.5,-2.77555756156289E-17));
#52579=CARTESIAN_POINT('',(-0.23094010767585,-0.5,-2.82820063659975E-17));
#52580=CARTESIAN_POINT('',(-0.115470053837925,-0.5,-0.2));
#52581=CARTESIAN_POINT('',(-0.23094010767585,-0.8,-2.77555756156289E-17));
#52582=CARTESIAN_POINT('',(-0.23094010767585,-0.5,-2.82820063659975E-17));
#52583=CARTESIAN_POINT('',(-0.115470053837925,-0.8,-0.2));
#52584=CARTESIAN_POINT('Origin',(-0.115470053837925,-0.5,0.2));
#52585=CARTESIAN_POINT('',(-0.115470053837925,-0.5,0.2));
#52586=CARTESIAN_POINT('',(-0.23094010767585,-0.5,-2.82820063659975E-17));
#52587=CARTESIAN_POINT('',(-0.115470053837925,-0.8,0.2));
#52588=CARTESIAN_POINT('',(-0.115470053837925,-0.5,0.2));
#52589=CARTESIAN_POINT('',(-0.23094010767585,-0.8,-2.82820063659975E-17));
#52590=CARTESIAN_POINT('Origin',(0.115470053837925,-0.5,0.2));
#52591=CARTESIAN_POINT('',(0.115470053837925,-0.5,0.2));
#52592=CARTESIAN_POINT('',(-0.115470053837925,-0.5,0.2));
#52593=CARTESIAN_POINT('',(0.115470053837925,-0.8,0.2));
#52594=CARTESIAN_POINT('',(0.115470053837925,-0.5,0.2));
#52595=CARTESIAN_POINT('',(-0.115470053837925,-0.8,0.2));
#52596=CARTESIAN_POINT('Origin',(0.23094010767585,-0.5,0.));
#52597=CARTESIAN_POINT('',(0.115470053837925,-0.5,0.2));
#52598=CARTESIAN_POINT('',(0.115470053837925,-0.8,0.2));
#52599=CARTESIAN_POINT('Origin',(0.,-0.5,0.));
#52600=CARTESIAN_POINT('Origin',(0.,-0.8,0.));
#62873=UNCERTAINTY_MEASURE_WITH_UNIT(LENGTH_MEASURE(0.001),#62985,
'DISTANCE_ACCURACY_VALUE',
'Maximum model space distance between geometric entities at asserted c
onnectivities');
#62885=UNCERTAINTY_MEASURE_WITH_UNIT(LENGTH_MEASURE(0.001),#62985,
'DISTANCE_ACCURACY_VALUE',
'Maximum model space distance between geometric entities at asserted c
onnectivities');
#62972=(
GEOMETRIC_REPRESENTATION_CONTEXT(3)
GLOBAL_UNCERTAINTY_ASSIGNED_CONTEXT((#62873))
GLOBAL_UNIT_ASSIGNED_CONTEXT((#62985,#62987,#62988))
REPRESENTATION_CONTEXT('','3D')
);
#62984=(
GEOMETRIC_REPRESENTATION_CONTEXT(3)
GLOBAL_UNCERTAINTY_ASSIGNED_CONTEXT((#62885))
GLOBAL_UNIT_ASSIGNED_CONTEXT((#62985,#62987,#62988))
REPRESENTATION_CONTEXT('','3D')
);
#62985=(
LENGTH_UNIT()
NAMED_UNIT(*)
SI_UNIT(.CENTI.,.METRE.)
);
#62987=(
NAMED_UNIT(*)
PLANE_ANGLE_UNIT()
SI_UNIT($,.RADIAN.)
);
#62988=(
NAMED_UNIT(*)
SI_UNIT($,.STERADIAN.)
SOLID_ANGLE_UNIT()
);
#63075=SHAPE_DEFINITION_REPRESENTATION(#63266,#63435);
#63266=PRODUCT_DEFINITION_SHAPE('',$,#63534);
#63435=SHAPE_REPRESENTATION('',(#26080),#62972);
#63447=PRODUCT_DEFINITION_CONTEXT('part definition',#63743,'design');
#63534=PRODUCT_DEFINITION('Cap Screw - M5x20 (1)','Cap Screw - M5x20 (1)',
#63632,#63447);
#63632=PRODUCT_DEFINITION_FORMATION('',$,#63831);
#63743=APPLICATION_CONTEXT(
'Core Data for Automotive Mechanical Design Process');
#63744=PRODUCT_CONTEXT('part definition',#63743,'mechanical');
#63831=PRODUCT('Cap Screw - M5x20 (1)','Cap Screw - M5x20 (1)',
'Cap Screw - M5x20 (1)',(#63744));
#63913=COLOUR_RGB('Black',0.12,0.14,0.17);
#63914=FILL_AREA_STYLE_COLOUR('',#63913);
#63915=FILL_AREA_STYLE('',(#63914));
#63916=SURFACE_STYLE_FILL_AREA(#63915);
#63917=SURFACE_SIDE_STYLE('',(#63916));
#63918=SURFACE_STYLE_USAGE(.BOTH.,#63917);
#63919=PRESENTATION_STYLE_ASSIGNMENT((#63918));
ENDSEC;
END-ISO-10303-21;
